ISO-10303-21;
HEADER;
/* Generated by software containing ST-Developer
 * from STEP Tools, Inc. (www.steptools.com) 
 */

FILE_DESCRIPTION(
/* description */ (''),
/* implementation_level */ '2;1');

FILE_NAME(
/* name */ 'PO12.step',
/* time_stamp */ '2026-10-06T10:18:54-07:00',
/* author */ (''),
/* organization */ (''),
/* preprocessor_version */ 'ST-DEVELOPER v20.2',
/* originating_system */ 'Autodesk Translation Framework v15.15.0.0',
/* authorisation */ '');

FILE_SCHEMA (('AUTOMOTIVE_DESIGN { 1 0 10303 214 3 1 1 }'));
ENDSEC;

DATA;
#10=MECHANICAL_DESIGN_GEOMETRIC_PRESENTATION_REPRESENTATION('',(#87),#8445);
#69=SHAPE_REPRESENTATION_RELATIONSHIP('SRR','None',#8490,#78);
#78=ADVANCED_BREP_SHAPE_REPRESENTATION('',(#96),#8442);
#87=STYLED_ITEM('',(#8537),#96);
#96=MANIFOLD_SOLID_BREP('Body1',#4008);
#160=CYLINDRICAL_SURFACE('',#4445,1.);
#161=CYLINDRICAL_SURFACE('',#4449,1.9);
#363=FACE_BOUND('',#996,.T.);
#498=CIRCLE('',#4438,1.9);
#499=CIRCLE('',#4439,1.9);
#500=CIRCLE('',#4441,1.9);
#501=CIRCLE('',#4442,1.9);
#502=CIRCLE('',#4444,1.9);
#503=CIRCLE('',#4446,1.);
#504=CIRCLE('',#4447,1.);
#505=CIRCLE('',#4450,1.9);
#726=FACE_OUTER_BOUND('',#987,.T.);
#727=FACE_OUTER_BOUND('',#988,.T.);
#728=FACE_OUTER_BOUND('',#989,.T.);
#729=FACE_OUTER_BOUND('',#990,.T.);
#730=FACE_OUTER_BOUND('',#991,.T.);
#731=FACE_OUTER_BOUND('',#992,.T.);
#732=FACE_OUTER_BOUND('',#993,.T.);
#733=FACE_OUTER_BOUND('',#994,.T.);
#734=FACE_OUTER_BOUND('',#995,.T.);
#987=EDGE_LOOP('',(#3515,#3516,#3517,#3518));
#988=EDGE_LOOP('',(#3519,#3520,#3521,#3522));
#989=EDGE_LOOP('',(#3523,#3524,#3525,#3526));
#990=EDGE_LOOP('',(#3527,#3528,#3529));
#991=EDGE_LOOP('',(#3530,#3531));
#992=EDGE_LOOP('',(#3532,#3533,#3534,#3535));
#993=EDGE_LOOP('',(#3536));
#994=EDGE_LOOP('',(#3537,#3538,#3539,#3540,#3541,#3542,#3543,#3544,#3545,
#3546,#3547,#3548));
#995=EDGE_LOOP('',(#3549));
#996=EDGE_LOOP('',(#3550));
#1276=LINE('',#8262,#1565);
#1277=LINE('',#8264,#1566);
#1278=LINE('',#8266,#1567);
#1279=LINE('',#8267,#1568);
#1280=LINE('',#8271,#1569);
#1281=LINE('',#8273,#1570);
#1282=LINE('',#8275,#1571);
#1283=LINE('',#8276,#1572);
#1284=LINE('',#8290,#1573);
#1285=LINE('',#8296,#1574);
#1565=VECTOR('',#5411,10.);
#1566=VECTOR('',#5412,10.);
#1567=VECTOR('',#5413,10.);
#1568=VECTOR('',#5414,10.);
#1569=VECTOR('',#5417,10.);
#1570=VECTOR('',#5418,10.);
#1571=VECTOR('',#5419,10.);
#1572=VECTOR('',#5420,10.);
#1573=VECTOR('',#5441,1.);
#1574=VECTOR('',#5450,1.9);
#1918=VERTEX_POINT('',#8260);
#1919=VERTEX_POINT('',#8261);
#1920=VERTEX_POINT('',#8263);
#1921=VERTEX_POINT('',#8265);
#1922=VERTEX_POINT('',#8269);
#1923=VERTEX_POINT('',#8270);
#1924=VERTEX_POINT('',#8272);
#1925=VERTEX_POINT('',#8274);
#1926=VERTEX_POINT('',#8281);
#1927=VERTEX_POINT('',#8287);
#1928=VERTEX_POINT('',#8289);
#1929=VERTEX_POINT('',#8294);
#2458=EDGE_CURVE('',#1918,#1919,#1276,.T.);
#2459=EDGE_CURVE('',#1920,#1918,#1277,.T.);
#2460=EDGE_CURVE('',#1920,#1921,#1278,.T.);
#2461=EDGE_CURVE('',#1919,#1921,#1279,.T.);
#2462=EDGE_CURVE('',#1922,#1923,#1280,.T.);
#2463=EDGE_CURVE('',#1924,#1922,#1281,.T.);
#2464=EDGE_CURVE('',#1924,#1925,#1282,.T.);
#2465=EDGE_CURVE('',#1923,#1925,#1283,.T.);
#2466=EDGE_CURVE('',#1921,#1924,#498,.T.);
#2467=EDGE_CURVE('',#1925,#1920,#499,.T.);
#2468=EDGE_CURVE('',#1926,#1923,#500,.T.);
#2469=EDGE_CURVE('',#1922,#1926,#501,.T.);
#2470=EDGE_CURVE('',#1918,#1919,#502,.T.);
#2471=EDGE_CURVE('',#1927,#1927,#503,.T.);
#2472=EDGE_CURVE('',#1927,#1928,#1284,.T.);
#2473=EDGE_CURVE('',#1928,#1928,#504,.T.);
#2474=EDGE_CURVE('',#1929,#1929,#505,.T.);
#2475=EDGE_CURVE('',#1929,#1926,#1285,.T.);
#3515=ORIENTED_EDGE('',*,*,#2458,.F.);
#3516=ORIENTED_EDGE('',*,*,#2459,.F.);
#3517=ORIENTED_EDGE('',*,*,#2460,.T.);
#3518=ORIENTED_EDGE('',*,*,#2461,.F.);
#3519=ORIENTED_EDGE('',*,*,#2462,.F.);
#3520=ORIENTED_EDGE('',*,*,#2463,.F.);
#3521=ORIENTED_EDGE('',*,*,#2464,.T.);
#3522=ORIENTED_EDGE('',*,*,#2465,.F.);
#3523=ORIENTED_EDGE('',*,*,#2466,.F.);
#3524=ORIENTED_EDGE('',*,*,#2460,.F.);
#3525=ORIENTED_EDGE('',*,*,#2467,.F.);
#3526=ORIENTED_EDGE('',*,*,#2464,.F.);
#3527=ORIENTED_EDGE('',*,*,#2462,.T.);
#3528=ORIENTED_EDGE('',*,*,#2468,.F.);
#3529=ORIENTED_EDGE('',*,*,#2469,.F.);
#3530=ORIENTED_EDGE('',*,*,#2458,.T.);
#3531=ORIENTED_EDGE('',*,*,#2470,.F.);
#3532=ORIENTED_EDGE('',*,*,#2471,.F.);
#3533=ORIENTED_EDGE('',*,*,#2472,.T.);
#3534=ORIENTED_EDGE('',*,*,#2473,.F.);
#3535=ORIENTED_EDGE('',*,*,#2472,.F.);
#3536=ORIENTED_EDGE('',*,*,#2471,.T.);
#3537=ORIENTED_EDGE('',*,*,#2474,.F.);
#3538=ORIENTED_EDGE('',*,*,#2475,.T.);
#3539=ORIENTED_EDGE('',*,*,#2468,.T.);
#3540=ORIENTED_EDGE('',*,*,#2465,.T.);
#3541=ORIENTED_EDGE('',*,*,#2467,.T.);
#3542=ORIENTED_EDGE('',*,*,#2459,.T.);
#3543=ORIENTED_EDGE('',*,*,#2470,.T.);
#3544=ORIENTED_EDGE('',*,*,#2461,.T.);
#3545=ORIENTED_EDGE('',*,*,#2466,.T.);
#3546=ORIENTED_EDGE('',*,*,#2463,.T.);
#3547=ORIENTED_EDGE('',*,*,#2469,.T.);
#3548=ORIENTED_EDGE('',*,*,#2475,.F.);
#3549=ORIENTED_EDGE('',*,*,#2474,.T.);
#3550=ORIENTED_EDGE('',*,*,#2473,.T.);
#3743=PLANE('',#4435);
#3744=PLANE('',#4436);
#3745=PLANE('',#4437);
#3746=PLANE('',#4440);
#3747=PLANE('',#4443);
#3748=PLANE('',#4448);
#3749=PLANE('',#4451);
#3967=ADVANCED_FACE('',(#726),#3743,.F.);
#3968=ADVANCED_FACE('',(#727),#3744,.F.);
#3969=ADVANCED_FACE('',(#728),#3745,.T.);
#3970=ADVANCED_FACE('',(#729),#3746,.F.);
#3971=ADVANCED_FACE('',(#730),#3747,.F.);
#3972=ADVANCED_FACE('',(#731),#160,.T.);
#3973=ADVANCED_FACE('',(#732),#3748,.T.);
#3974=ADVANCED_FACE('',(#733),#161,.T.);
#3975=ADVANCED_FACE('',(#734,#363),#3749,.T.);
#4008=CLOSED_SHELL('',(#3967,#3968,#3969,#3970,#3971,#3972,#3973,#3974,
#3975));
#4434=AXIS2_PLACEMENT_3D('',#8258,#5407,#5408);
#4435=AXIS2_PLACEMENT_3D('',#8259,#5409,#5410);
#4436=AXIS2_PLACEMENT_3D('',#8268,#5415,#5416);
#4437=AXIS2_PLACEMENT_3D('',#8277,#5421,#5422);
#4438=AXIS2_PLACEMENT_3D('',#8278,#5423,#5424);
#4439=AXIS2_PLACEMENT_3D('',#8279,#5425,#5426);
#4440=AXIS2_PLACEMENT_3D('',#8280,#5427,#5428);
#4441=AXIS2_PLACEMENT_3D('',#8282,#5429,#5430);
#4442=AXIS2_PLACEMENT_3D('',#8283,#5431,#5432);
#4443=AXIS2_PLACEMENT_3D('',#8284,#5433,#5434);
#4444=AXIS2_PLACEMENT_3D('',#8285,#5435,#5436);
#4445=AXIS2_PLACEMENT_3D('',#8286,#5437,#5438);
#4446=AXIS2_PLACEMENT_3D('',#8288,#5439,#5440);
#4447=AXIS2_PLACEMENT_3D('',#8291,#5442,#5443);
#4448=AXIS2_PLACEMENT_3D('',#8292,#5444,#5445);
#4449=AXIS2_PLACEMENT_3D('',#8293,#5446,#5447);
#4450=AXIS2_PLACEMENT_3D('',#8295,#5448,#5449);
#4451=AXIS2_PLACEMENT_3D('',#8297,#5451,#5452);
#5407=DIRECTION('axis',(0.,0.,1.));
#5408=DIRECTION('refdir',(1.,0.,0.));
#5409=DIRECTION('center_axis',(0.,1.,0.));
#5410=DIRECTION('ref_axis',(0.,0.,1.));
#5411=DIRECTION('',(0.,0.,1.));
#5412=DIRECTION('',(-1.,0.,0.));
#5413=DIRECTION('',(0.,0.,1.));
#5414=DIRECTION('',(1.,0.,0.));
#5415=DIRECTION('center_axis',(0.,-1.,0.));
#5416=DIRECTION('ref_axis',(0.,0.,-1.));
#5417=DIRECTION('',(0.,0.,-1.));
#5418=DIRECTION('',(-1.,0.,0.));
#5419=DIRECTION('',(0.,0.,-1.));
#5420=DIRECTION('',(1.,0.,0.));
#5421=DIRECTION('center_axis',(-1.,0.,0.));
#5422=DIRECTION('ref_axis',(0.,-1.,0.));
#5423=DIRECTION('center_axis',(1.,0.,0.));
#5424=DIRECTION('ref_axis',(0.,1.,0.));
#5425=DIRECTION('center_axis',(1.,0.,0.));
#5426=DIRECTION('ref_axis',(0.,1.,0.));
#5427=DIRECTION('center_axis',(1.,0.,0.));
#5428=DIRECTION('ref_axis',(0.,1.,0.));
#5429=DIRECTION('center_axis',(1.,0.,0.));
#5430=DIRECTION('ref_axis',(0.,1.,0.));
#5431=DIRECTION('center_axis',(1.,0.,0.));
#5432=DIRECTION('ref_axis',(0.,1.,0.));
#5433=DIRECTION('center_axis',(1.,0.,0.));
#5434=DIRECTION('ref_axis',(0.,1.,0.));
#5435=DIRECTION('center_axis',(1.,0.,0.));
#5436=DIRECTION('ref_axis',(0.,1.,0.));
#5437=DIRECTION('center_axis',(1.,0.,0.));
#5438=DIRECTION('ref_axis',(0.,1.,0.));
#5439=DIRECTION('center_axis',(1.,0.,0.));
#5440=DIRECTION('ref_axis',(0.,1.,0.));
#5441=DIRECTION('',(-1.,0.,0.));
#5442=DIRECTION('center_axis',(-1.,0.,0.));
#5443=DIRECTION('ref_axis',(0.,1.,0.));
#5444=DIRECTION('center_axis',(1.,0.,0.));
#5445=DIRECTION('ref_axis',(0.,1.,0.));
#5446=DIRECTION('center_axis',(1.,0.,0.));
#5447=DIRECTION('ref_axis',(0.,1.,0.));
#5448=DIRECTION('center_axis',(1.,0.,0.));
#5449=DIRECTION('ref_axis',(0.,1.,0.));
#5450=DIRECTION('',(-1.,0.,0.));
#5451=DIRECTION('center_axis',(1.,0.,0.));
#5452=DIRECTION('ref_axis',(0.,1.,0.));
#8258=CARTESIAN_POINT('',(0.,0.,0.));
#8259=CARTESIAN_POINT('Origin',(0.,0.35,-1.86748493969831));
#8260=CARTESIAN_POINT('',(0.,0.35,-1.86748493969831));
#8261=CARTESIAN_POINT('',(0.,0.35,1.86748493969831));
#8262=CARTESIAN_POINT('',(0.,0.35,-0.933742469849155));
#8263=CARTESIAN_POINT('',(0.5,0.35,-1.86748493969831));
#8264=CARTESIAN_POINT('',(0.,0.35,-1.86748493969831));
#8265=CARTESIAN_POINT('',(0.5,0.35,1.86748493969831));
#8266=CARTESIAN_POINT('',(0.5,0.35,0.));
#8267=CARTESIAN_POINT('',(0.,0.35,1.86748493969831));
#8268=CARTESIAN_POINT('Origin',(0.,-0.35,1.86748493969831));
#8269=CARTESIAN_POINT('',(0.,-0.35,1.86748493969831));
#8270=CARTESIAN_POINT('',(0.,-0.35,-1.86748493969831));
#8271=CARTESIAN_POINT('',(0.,-0.35,0.933742469849155));
#8272=CARTESIAN_POINT('',(0.5,-0.35,1.86748493969831));
#8273=CARTESIAN_POINT('',(0.,-0.35,1.86748493969831));
#8274=CARTESIAN_POINT('',(0.5,-0.35,-1.86748493969831));
#8275=CARTESIAN_POINT('',(0.5,-0.35,0.));
#8276=CARTESIAN_POINT('',(0.,-0.35,-1.86748493969831));
#8277=CARTESIAN_POINT('Origin',(0.5,0.,0.));
#8278=CARTESIAN_POINT('Origin',(0.5,0.,0.));
#8279=CARTESIAN_POINT('Origin',(0.5,0.,0.));
#8280=CARTESIAN_POINT('Origin',(0.,0.,0.));
#8281=CARTESIAN_POINT('',(0.,-1.9,-2.32682891837997E-16));
#8282=CARTESIAN_POINT('Origin',(0.,0.,0.));
#8283=CARTESIAN_POINT('Origin',(0.,0.,0.));
#8284=CARTESIAN_POINT('Origin',(0.,0.,0.));
#8285=CARTESIAN_POINT('Origin',(0.,0.,0.));
#8286=CARTESIAN_POINT('Origin',(1.3,0.,0.));
#8287=CARTESIAN_POINT('',(11.3,-1.,-1.22464679914735E-16));
#8288=CARTESIAN_POINT('Origin',(11.3,0.,0.));
#8289=CARTESIAN_POINT('',(1.3,-1.,-1.22464679914735E-16));
#8290=CARTESIAN_POINT('',(1.3,-1.,-1.22464679914735E-16));
#8291=CARTESIAN_POINT('Origin',(1.3,0.,0.));
#8292=CARTESIAN_POINT('Origin',(11.3,0.,0.));
#8293=CARTESIAN_POINT('Origin',(0.,0.,0.));
#8294=CARTESIAN_POINT('',(1.3,-1.9,-2.32682891837997E-16));
#8295=CARTESIAN_POINT('Origin',(1.3,0.,0.));
#8296=CARTESIAN_POINT('',(0.,-1.9,-2.32682891837997E-16));
#8297=CARTESIAN_POINT('Origin',(1.3,0.,0.));
#8431=UNCERTAINTY_MEASURE_WITH_UNIT(LENGTH_MEASURE(0.01),#8446,
'DISTANCE_ACCURACY_VALUE',
'Maximum model space distance between geometric entities at asserted c
onnectivities');
#8434=UNCERTAINTY_MEASURE_WITH_UNIT(LENGTH_MEASURE(0.01),#8446,
'DISTANCE_ACCURACY_VALUE',
'Maximum model space distance between geometric entities at asserted c
onnectivities');
#8442=(
GEOMETRIC_REPRESENTATION_CONTEXT(3)
GLOBAL_UNCERTAINTY_ASSIGNED_CONTEXT((#8431))
GLOBAL_UNIT_ASSIGNED_CONTEXT((#8446,#8448,#8449))
REPRESENTATION_CONTEXT('','3D')
);
#8445=(
GEOMETRIC_REPRESENTATION_CONTEXT(3)
GLOBAL_UNCERTAINTY_ASSIGNED_CONTEXT((#8434))
GLOBAL_UNIT_ASSIGNED_CONTEXT((#8446,#8448,#8449))
REPRESENTATION_CONTEXT('','3D')
);
#8446=(
LENGTH_UNIT()
NAMED_UNIT(*)
SI_UNIT(.MILLI.,.METRE.)
);
#8448=(
NAMED_UNIT(*)
PLANE_ANGLE_UNIT()
SI_UNIT($,.RADIAN.)
);
#8449=(
NAMED_UNIT(*)
SI_UNIT($,.STERADIAN.)
SOLID_ANGLE_UNIT()
);
#8457=SHAPE_DEFINITION_REPRESENTATION(#8467,#8490);
#8467=PRODUCT_DEFINITION_SHAPE('',$,#8501);
#8490=SHAPE_REPRESENTATION('',(#4434),#8442);
#8493=PRODUCT_DEFINITION_CONTEXT('part definition',#8525,'design');
#8501=PRODUCT_DEFINITION('2026-10-05-11-51-05-164','PO12',#8511,#8493);
#8511=PRODUCT_DEFINITION_FORMATION('',$,#8534);
#8525=APPLICATION_CONTEXT(
'Core Data for Automotive Mechanical Design Process');
#8526=PRODUCT_CONTEXT('part definition',#8525,'mechanical');
#8534=PRODUCT('2026-10-05-11-51-05-164','PO12',$,(#8526));
#8537=PRESENTATION_STYLE_ASSIGNMENT((#8538));
#8538=SURFACE_STYLE_USAGE(.BOTH.,#8539);
#8539=SURFACE_SIDE_STYLE('',(#8540));
#8540=SURFACE_STYLE_FILL_AREA(#8541);
#8541=FILL_AREA_STYLE('Steel - Satin',(#8542));
#8542=FILL_AREA_STYLE_COLOUR('Steel - Satin',#8543);
#8543=COLOUR_RGB('Steel - Satin', 0.09019608, 0.27058824, 0.51372549);
ENDSEC;
END-ISO-10303-21;
